ISO-10303-21;
HEADER;
/* Generated by software containing ST-Developer
 * from STEP Tools, Inc. (www.steptools.com) 
 */

FILE_DESCRIPTION(
/* description */ ('Flywheel Crank-Slider'),
/* implementation_level */ '2;1');

FILE_NAME(
/* name */ 'M5x14 Cap Screw.step',
/* time_stamp */ '2026-10-28T03:23:13-07:00',
/* author */ (''),
/* organization */ (''),
/* preprocessor_version */ 'ST-DEVELOPER v20.2',
/* originating_system */ 'Autodesk Translation Framework v15.17.0.0',
/* authorisation */ '');

FILE_SCHEMA (('AUTOMOTIVE_DESIGN { 1 0 10303 214 3 1 1 }'));
ENDSEC;

DATA;
#10=MECHANICAL_DESIGN_GEOMETRIC_PRESENTATION_REPRESENTATION('',(#687),#17322);
#531=ORIENTED_CLOSED_SHELL('',*,#9067,.F.);
#542=CONICAL_SURFACE('',#10139,0.4,0.785398163397448);
#543=CONICAL_SURFACE('',#10143,0.41,0.785398163397448);
#544=CONICAL_SURFACE('',#10147,0.26,0.463647609000806);
#561=BREP_WITH_VOIDS('Body1',#9068,(#531));
#582=SHAPE_REPRESENTATION_RELATIONSHIP('SRR','None',#17579,#634);
#634=ADVANCED_BREP_SHAPE_REPRESENTATION('',(#561),#17283);
#687=STYLED_ITEM('',(#17938),#561);
#906=FACE_BOUND('',#2228,.T.);
#1151=PLANE('',#10127);
#1152=PLANE('',#10128);
#1153=PLANE('',#10129);
#1154=PLANE('',#10130);
#1155=PLANE('',#10131);
#1156=PLANE('',#10132);
#1157=PLANE('',#10133);
#1158=PLANE('',#10134);
#1159=PLANE('',#10135);
#1160=PLANE('',#10137);
#1161=PLANE('',#10145);
#1558=FACE_OUTER_BOUND('',#2214,.T.);
#1559=FACE_OUTER_BOUND('',#2215,.T.);
#1560=FACE_OUTER_BOUND('',#2216,.T.);
#1561=FACE_OUTER_BOUND('',#2217,.T.);
#1562=FACE_OUTER_BOUND('',#2218,.T.);
#1563=FACE_OUTER_BOUND('',#2219,.T.);
#1564=FACE_OUTER_BOUND('',#2220,.T.);
#1565=FACE_OUTER_BOUND('',#2221,.T.);
#1566=FACE_OUTER_BOUND('',#2222,.T.);
#1567=FACE_OUTER_BOUND('',#2223,.T.);
#1568=FACE_OUTER_BOUND('',#2224,.T.);
#1569=FACE_OUTER_BOUND('',#2225,.T.);
#1570=FACE_OUTER_BOUND('',#2226,.T.);
#1571=FACE_OUTER_BOUND('',#2227,.T.);
#1572=FACE_OUTER_BOUND('',#2229,.T.);
#1573=FACE_OUTER_BOUND('',#2230,.T.);
#2214=EDGE_LOOP('',(#7144,#7145,#7146,#7147));
#2215=EDGE_LOOP('',(#7148,#7149,#7150,#7151));
#2216=EDGE_LOOP('',(#7152,#7153,#7154,#7155));
#2217=EDGE_LOOP('',(#7156,#7157,#7158,#7159));
#2218=EDGE_LOOP('',(#7160,#7161,#7162,#7163));
#2219=EDGE_LOOP('',(#7164,#7165,#7166,#7167));
#2220=EDGE_LOOP('',(#7168,#7169,#7170,#7171,#7172,#7173));
#2221=EDGE_LOOP('',(#7174,#7175,#7176,#7177,#7178,#7179));
#2222=EDGE_LOOP('',(#7180));
#2223=EDGE_LOOP('',(#7181));
#2224=EDGE_LOOP('',(#7182,#7183,#7184,#7185));
#2225=EDGE_LOOP('',(#7186,#7187,#7188,#7189));
#2226=EDGE_LOOP('',(#7190,#7191,#7192,#7193));
#2227=EDGE_LOOP('',(#7194));
#2228=EDGE_LOOP('',(#7195));
#2229=EDGE_LOOP('',(#7196,#7197,#7198,#7199));
#2230=EDGE_LOOP('',(#7200,#7201,#7202,#7203));
#2923=LINE('',#15255,#3534);
#2924=LINE('',#15257,#3535);
#2925=LINE('',#15259,#3536);
#2926=LINE('',#15260,#3537);
#2927=LINE('',#15263,#3538);
#2928=LINE('',#15265,#3539);
#2929=LINE('',#15266,#3540);
#2930=LINE('',#15269,#3541);
#2931=LINE('',#15271,#3542);
#2932=LINE('',#15272,#3543);
#2933=LINE('',#15275,#3544);
#2934=LINE('',#15277,#3545);
#2935=LINE('',#15278,#3546);
#2936=LINE('',#15281,#3547);
#2937=LINE('',#15283,#3548);
#2938=LINE('',#15284,#3549);
#2939=LINE('',#15286,#3550);
#2940=LINE('',#15287,#3551);
#2941=LINE('',#15299,#3552);
#2942=LINE('',#15303,#3553);
#2943=LINE('',#15307,#3554);
#2944=LINE('',#15314,#3555);
#2945=LINE('',#15316,#3556);
#3534=VECTOR('',#12023,1.);
#3535=VECTOR('',#12024,1.);
#3536=VECTOR('',#12025,1.);
#3537=VECTOR('',#12026,1.);
#3538=VECTOR('',#12029,1.);
#3539=VECTOR('',#12030,1.);
#3540=VECTOR('',#12031,1.);
#3541=VECTOR('',#12034,1.);
#3542=VECTOR('',#12035,1.);
#3543=VECTOR('',#12036,1.);
#3544=VECTOR('',#12039,1.);
#3545=VECTOR('',#12040,1.);
#3546=VECTOR('',#12041,1.);
#3547=VECTOR('',#12044,1.);
#3548=VECTOR('',#12045,1.);
#3549=VECTOR('',#12046,1.);
#3550=VECTOR('',#12049,1.);
#3551=VECTOR('',#12050,1.);
#3552=VECTOR('',#12067,0.4);
#3553=VECTOR('',#12072,0.425);
#3554=VECTOR('',#12077,0.41);
#3555=VECTOR('',#12086,0.26);
#3556=VECTOR('',#12089,0.25);
#4018=CIRCLE('',#10136,0.24505);
#4019=CIRCLE('',#10138,0.375);
#4020=CIRCLE('',#10140,0.425);
#4021=CIRCLE('',#10142,0.425);
#4022=CIRCLE('',#10144,0.395);
#4023=CIRCLE('',#10146,0.27);
#4024=CIRCLE('',#10148,0.24505);
#4617=VERTEX_POINT('',#15253);
#4618=VERTEX_POINT('',#15254);
#4619=VERTEX_POINT('',#15256);
#4620=VERTEX_POINT('',#15258);
#4621=VERTEX_POINT('',#15262);
#4622=VERTEX_POINT('',#15264);
#4623=VERTEX_POINT('',#15268);
#4624=VERTEX_POINT('',#15270);
#4625=VERTEX_POINT('',#15274);
#4626=VERTEX_POINT('',#15276);
#4627=VERTEX_POINT('',#15280);
#4628=VERTEX_POINT('',#15282);
#4629=VERTEX_POINT('',#15291);
#4630=VERTEX_POINT('',#15294);
#4631=VERTEX_POINT('',#15297);
#4632=VERTEX_POINT('',#15301);
#4633=VERTEX_POINT('',#15305);
#4634=VERTEX_POINT('',#15309);
#4635=VERTEX_POINT('',#15312);
#5529=EDGE_CURVE('',#4617,#4618,#2923,.T.);
#5530=EDGE_CURVE('',#4618,#4619,#2924,.T.);
#5531=EDGE_CURVE('',#4619,#4620,#2925,.T.);
#5532=EDGE_CURVE('',#4617,#4620,#2926,.T.);
#5533=EDGE_CURVE('',#4618,#4621,#2927,.T.);
#5534=EDGE_CURVE('',#4621,#4622,#2928,.T.);
#5535=EDGE_CURVE('',#4622,#4619,#2929,.T.);
#5536=EDGE_CURVE('',#4621,#4623,#2930,.T.);
#5537=EDGE_CURVE('',#4623,#4624,#2931,.T.);
#5538=EDGE_CURVE('',#4624,#4622,#2932,.T.);
#5539=EDGE_CURVE('',#4623,#4625,#2933,.T.);
#5540=EDGE_CURVE('',#4625,#4626,#2934,.T.);
#5541=EDGE_CURVE('',#4626,#4624,#2935,.T.);
#5542=EDGE_CURVE('',#4625,#4627,#2936,.T.);
#5543=EDGE_CURVE('',#4627,#4628,#2937,.T.);
#5544=EDGE_CURVE('',#4628,#4626,#2938,.T.);
#5545=EDGE_CURVE('',#4627,#4617,#2939,.T.);
#5546=EDGE_CURVE('',#4620,#4628,#2940,.T.);
#5547=EDGE_CURVE('',#4629,#4629,#4018,.T.);
#5548=EDGE_CURVE('',#4630,#4630,#4019,.T.);
#5549=EDGE_CURVE('',#4631,#4631,#4020,.T.);
#5550=EDGE_CURVE('',#4631,#4630,#2941,.T.);
#5551=EDGE_CURVE('',#4632,#4632,#4021,.T.);
#5552=EDGE_CURVE('',#4632,#4631,#2942,.T.);
#5553=EDGE_CURVE('',#4633,#4633,#4022,.T.);
#5554=EDGE_CURVE('',#4633,#4632,#2943,.T.);
#5555=EDGE_CURVE('',#4634,#4634,#4023,.T.);
#5556=EDGE_CURVE('',#4635,#4635,#4024,.F.);
#5557=EDGE_CURVE('',#4635,#4634,#2944,.T.);
#5558=EDGE_CURVE('',#4629,#4635,#2945,.T.);
#7144=ORIENTED_EDGE('',*,*,#5529,.T.);
#7145=ORIENTED_EDGE('',*,*,#5530,.T.);
#7146=ORIENTED_EDGE('',*,*,#5531,.T.);
#7147=ORIENTED_EDGE('',*,*,#5532,.F.);
#7148=ORIENTED_EDGE('',*,*,#5533,.T.);
#7149=ORIENTED_EDGE('',*,*,#5534,.T.);
#7150=ORIENTED_EDGE('',*,*,#5535,.T.);
#7151=ORIENTED_EDGE('',*,*,#5530,.F.);
#7152=ORIENTED_EDGE('',*,*,#5536,.T.);
#7153=ORIENTED_EDGE('',*,*,#5537,.T.);
#7154=ORIENTED_EDGE('',*,*,#5538,.T.);
#7155=ORIENTED_EDGE('',*,*,#5534,.F.);
#7156=ORIENTED_EDGE('',*,*,#5539,.T.);
#7157=ORIENTED_EDGE('',*,*,#5540,.T.);
#7158=ORIENTED_EDGE('',*,*,#5541,.T.);
#7159=ORIENTED_EDGE('',*,*,#5537,.F.);
#7160=ORIENTED_EDGE('',*,*,#5542,.T.);
#7161=ORIENTED_EDGE('',*,*,#5543,.T.);
#7162=ORIENTED_EDGE('',*,*,#5544,.T.);
#7163=ORIENTED_EDGE('',*,*,#5540,.F.);
#7164=ORIENTED_EDGE('',*,*,#5545,.T.);
#7165=ORIENTED_EDGE('',*,*,#5532,.T.);
#7166=ORIENTED_EDGE('',*,*,#5546,.T.);
#7167=ORIENTED_EDGE('',*,*,#5543,.F.);
#7168=ORIENTED_EDGE('',*,*,#5545,.F.);
#7169=ORIENTED_EDGE('',*,*,#5542,.F.);
#7170=ORIENTED_EDGE('',*,*,#5539,.F.);
#7171=ORIENTED_EDGE('',*,*,#5536,.F.);
#7172=ORIENTED_EDGE('',*,*,#5533,.F.);
#7173=ORIENTED_EDGE('',*,*,#5529,.F.);
#7174=ORIENTED_EDGE('',*,*,#5546,.F.);
#7175=ORIENTED_EDGE('',*,*,#5531,.F.);
#7176=ORIENTED_EDGE('',*,*,#5535,.F.);
#7177=ORIENTED_EDGE('',*,*,#5538,.F.);
#7178=ORIENTED_EDGE('',*,*,#5541,.F.);
#7179=ORIENTED_EDGE('',*,*,#5544,.F.);
#7180=ORIENTED_EDGE('',*,*,#5547,.F.);
#7181=ORIENTED_EDGE('',*,*,#5548,.F.);
#7182=ORIENTED_EDGE('',*,*,#5549,.F.);
#7183=ORIENTED_EDGE('',*,*,#5550,.T.);
#7184=ORIENTED_EDGE('',*,*,#5548,.T.);
#7185=ORIENTED_EDGE('',*,*,#5550,.F.);
#7186=ORIENTED_EDGE('',*,*,#5551,.F.);
#7187=ORIENTED_EDGE('',*,*,#5552,.T.);
#7188=ORIENTED_EDGE('',*,*,#5549,.T.);
#7189=ORIENTED_EDGE('',*,*,#5552,.F.);
#7190=ORIENTED_EDGE('',*,*,#5553,.F.);
#7191=ORIENTED_EDGE('',*,*,#5554,.T.);
#7192=ORIENTED_EDGE('',*,*,#5551,.T.);
#7193=ORIENTED_EDGE('',*,*,#5554,.F.);
#7194=ORIENTED_EDGE('',*,*,#5553,.T.);
#7195=ORIENTED_EDGE('',*,*,#5555,.F.);
#7196=ORIENTED_EDGE('',*,*,#5556,.F.);
#7197=ORIENTED_EDGE('',*,*,#5557,.T.);
#7198=ORIENTED_EDGE('',*,*,#5555,.T.);
#7199=ORIENTED_EDGE('',*,*,#5557,.F.);
#7200=ORIENTED_EDGE('',*,*,#5547,.T.);
#7201=ORIENTED_EDGE('',*,*,#5558,.T.);
#7202=ORIENTED_EDGE('',*,*,#5556,.T.);
#7203=ORIENTED_EDGE('',*,*,#5558,.F.);
#8418=CYLINDRICAL_SURFACE('',#10141,0.425);
#8419=CYLINDRICAL_SURFACE('',#10149,0.24505);
#8749=ADVANCED_FACE('',(#1558),#1151,.F.);
#8750=ADVANCED_FACE('',(#1559),#1152,.F.);
#8751=ADVANCED_FACE('',(#1560),#1153,.F.);
#8752=ADVANCED_FACE('',(#1561),#1154,.F.);
#8753=ADVANCED_FACE('',(#1562),#1155,.F.);
#8754=ADVANCED_FACE('',(#1563),#1156,.F.);
#8755=ADVANCED_FACE('',(#1564),#1157,.F.);
#8756=ADVANCED_FACE('',(#1565),#1158,.F.);
#8757=ADVANCED_FACE('',(#1566),#1159,.F.);
#8758=ADVANCED_FACE('',(#1567),#1160,.T.);
#8759=ADVANCED_FACE('',(#1568),#542,.T.);
#8760=ADVANCED_FACE('',(#1569),#8418,.T.);
#8761=ADVANCED_FACE('',(#1570),#543,.T.);
#8762=ADVANCED_FACE('',(#1571,#906),#1161,.T.);
#8763=ADVANCED_FACE('',(#1572),#544,.T.);
#8764=ADVANCED_FACE('',(#1573),#8419,.T.);
#9067=CLOSED_SHELL('',(#8749,#8750,#8751,#8752,#8753,#8754,#8755,#8756));
#9068=CLOSED_SHELL('',(#8757,#8758,#8759,#8760,#8761,#8762,#8763,#8764));
#10126=AXIS2_PLACEMENT_3D('',#15251,#12019,#12020);
#10127=AXIS2_PLACEMENT_3D('',#15252,#12021,#12022);
#10128=AXIS2_PLACEMENT_3D('',#15261,#12027,#12028);
#10129=AXIS2_PLACEMENT_3D('',#15267,#12032,#12033);
#10130=AXIS2_PLACEMENT_3D('',#15273,#12037,#12038);
#10131=AXIS2_PLACEMENT_3D('',#15279,#12042,#12043);
#10132=AXIS2_PLACEMENT_3D('',#15285,#12047,#12048);
#10133=AXIS2_PLACEMENT_3D('',#15288,#12051,#12052);
#10134=AXIS2_PLACEMENT_3D('',#15289,#12053,#12054);
#10135=AXIS2_PLACEMENT_3D('',#15290,#12055,#12056);
#10136=AXIS2_PLACEMENT_3D('',#15292,#12057,#12058);
#10137=AXIS2_PLACEMENT_3D('',#15293,#12059,#12060);
#10138=AXIS2_PLACEMENT_3D('',#15295,#12061,#12062);
#10139=AXIS2_PLACEMENT_3D('',#15296,#12063,#12064);
#10140=AXIS2_PLACEMENT_3D('',#15298,#12065,#12066);
#10141=AXIS2_PLACEMENT_3D('',#15300,#12068,#12069);
#10142=AXIS2_PLACEMENT_3D('',#15302,#12070,#12071);
#10143=AXIS2_PLACEMENT_3D('',#15304,#12073,#12074);
#10144=AXIS2_PLACEMENT_3D('',#15306,#12075,#12076);
#10145=AXIS2_PLACEMENT_3D('',#15308,#12078,#12079);
#10146=AXIS2_PLACEMENT_3D('',#15310,#12080,#12081);
#10147=AXIS2_PLACEMENT_3D('',#15311,#12082,#12083);
#10148=AXIS2_PLACEMENT_3D('',#15313,#12084,#12085);
#10149=AXIS2_PLACEMENT_3D('',#15315,#12087,#12088);
#12019=DIRECTION('axis',(0.,0.,1.));
#12020=DIRECTION('refdir',(1.,0.,0.));
#12021=DIRECTION('center_axis',(0.866025403784439,0.,-0.5));
#12022=DIRECTION('ref_axis',(0.5,0.,0.866025403784439));
#12023=DIRECTION('',(-0.5,0.,-0.866025403784439));
#12024=DIRECTION('',(0.,-1.,0.));
#12025=DIRECTION('',(0.5,0.,0.866025403784439));
#12026=DIRECTION('',(0.,-1.,0.));
#12027=DIRECTION('center_axis',(1.20185167898973E-16,0.,-1.));
#12028=DIRECTION('ref_axis',(1.,0.,1.20185167898973E-16));
#12029=DIRECTION('',(-1.,0.,-1.20185167898973E-16));
#12030=DIRECTION('',(0.,-1.,0.));
#12031=DIRECTION('',(1.,0.,1.20185167898973E-16));
#12032=DIRECTION('center_axis',(-0.866025403784439,0.,-0.5));
#12033=DIRECTION('ref_axis',(0.5,0.,-0.866025403784439));
#12034=DIRECTION('',(-0.5,0.,0.866025403784439));
#12035=DIRECTION('',(0.,-1.,0.));
#12036=DIRECTION('',(0.5,0.,-0.866025403784439));
#12037=DIRECTION('center_axis',(-0.866025403784439,0.,0.5));
#12038=DIRECTION('ref_axis',(-0.5,0.,-0.866025403784439));
#12039=DIRECTION('',(0.5,0.,0.866025403784439));
#12040=DIRECTION('',(0.,-1.,0.));
#12041=DIRECTION('',(-0.5,0.,-0.866025403784439));
#12042=DIRECTION('center_axis',(-2.40370335797945E-16,0.,1.));
#12043=DIRECTION('ref_axis',(-1.,0.,-2.40370335797945E-16));
#12044=DIRECTION('',(1.,0.,2.40370335797945E-16));
#12045=DIRECTION('',(0.,-1.,0.));
#12046=DIRECTION('',(-1.,0.,-2.40370335797945E-16));
#12047=DIRECTION('center_axis',(0.866025403784439,0.,0.5));
#12048=DIRECTION('ref_axis',(-0.5,0.,0.866025403784439));
#12049=DIRECTION('',(0.5,0.,-0.866025403784439));
#12050=DIRECTION('',(-0.5,0.,0.866025403784439));
#12051=DIRECTION('center_axis',(0.,1.,0.));
#12052=DIRECTION('ref_axis',(1.,0.,0.));
#12053=DIRECTION('center_axis',(0.,-1.,0.));
#12054=DIRECTION('ref_axis',(0.,0.,-1.));
#12055=DIRECTION('center_axis',(0.,1.,0.));
#12056=DIRECTION('ref_axis',(1.,0.,0.));
#12057=DIRECTION('center_axis',(0.,1.,0.));
#12058=DIRECTION('ref_axis',(1.,0.,0.));
#12059=DIRECTION('center_axis',(0.,1.,0.));
#12060=DIRECTION('ref_axis',(0.,0.,1.));
#12061=DIRECTION('center_axis',(0.,-1.,0.));
#12062=DIRECTION('ref_axis',(1.,0.,0.));
#12063=DIRECTION('center_axis',(0.,-1.,0.));
#12064=DIRECTION('ref_axis',(1.,0.,0.));
#12065=DIRECTION('center_axis',(0.,-1.,0.));
#12066=DIRECTION('ref_axis',(1.,0.,0.));
#12067=DIRECTION('',(0.707106781186548,0.707106781186547,8.65956056235493E-17));
#12068=DIRECTION('center_axis',(0.,-1.,0.));
#12069=DIRECTION('ref_axis',(1.,0.,0.));
#12070=DIRECTION('center_axis',(0.,-1.,0.));
#12071=DIRECTION('ref_axis',(1.,0.,0.));
#12072=DIRECTION('',(0.,1.,0.));
#12073=DIRECTION('center_axis',(0.,1.,0.));
#12074=DIRECTION('ref_axis',(1.,0.,0.));
#12075=DIRECTION('center_axis',(0.,-1.,0.));
#12076=DIRECTION('ref_axis',(1.,0.,0.));
#12077=DIRECTION('',(-0.707106781186547,0.707106781186548,-8.65956056235493E-17));
#12078=DIRECTION('center_axis',(0.,-1.,0.));
#12079=DIRECTION('ref_axis',(0.,0.,-1.));
#12080=DIRECTION('center_axis',(0.,-1.,0.));
#12081=DIRECTION('ref_axis',(1.,0.,0.));
#12082=DIRECTION('center_axis',(0.,1.,0.));
#12083=DIRECTION('ref_axis',(1.,0.,0.));
#12084=DIRECTION('center_axis',(0.,1.,0.));
#12085=DIRECTION('ref_axis',(1.,0.,0.));
#12086=DIRECTION('',(-0.447213595499958,0.894427190999916,-5.47678698264203E-17));
#12087=DIRECTION('center_axis',(0.,-1.,0.));
#12088=DIRECTION('ref_axis',(1.,0.,0.));
#12089=DIRECTION('',(0.,1.,0.));
#15251=CARTESIAN_POINT('',(0.,0.,0.));
#15252=CARTESIAN_POINT('Origin',(0.115470053837925,-0.5,-0.2));
#15253=CARTESIAN_POINT('',(0.23094010767585,-0.5,0.));
#15254=CARTESIAN_POINT('',(0.115470053837925,-0.5,-0.2));
#15255=CARTESIAN_POINT('',(0.23094010767585,-0.5,0.));
#15256=CARTESIAN_POINT('',(0.115470053837925,-0.8,-0.2));
#15257=CARTESIAN_POINT('',(0.115470053837925,-0.5,-0.2));
#15258=CARTESIAN_POINT('',(0.23094010767585,-0.8,0.));
#15259=CARTESIAN_POINT('',(0.23094010767585,-0.8,0.));
#15260=CARTESIAN_POINT('',(0.23094010767585,-0.5,0.));
#15261=CARTESIAN_POINT('Origin',(-0.115470053837925,-0.5,-0.2));
#15262=CARTESIAN_POINT('',(-0.115470053837925,-0.5,-0.2));
#15263=CARTESIAN_POINT('',(0.115470053837925,-0.5,-0.2));
#15264=CARTESIAN_POINT('',(-0.115470053837925,-0.8,-0.2));
#15265=CARTESIAN_POINT('',(-0.115470053837925,-0.5,-0.2));
#15266=CARTESIAN_POINT('',(0.115470053837925,-0.8,-0.2));
#15267=CARTESIAN_POINT('Origin',(-0.23094010767585,-0.5,-2.77555756156289E-17));
#15268=CARTESIAN_POINT('',(-0.23094010767585,-0.5,-2.82820063659975E-17));
#15269=CARTESIAN_POINT('',(-0.115470053837925,-0.5,-0.2));
#15270=CARTESIAN_POINT('',(-0.23094010767585,-0.8,-2.77555756156289E-17));
#15271=CARTESIAN_POINT('',(-0.23094010767585,-0.5,-2.82820063659975E-17));
#15272=CARTESIAN_POINT('',(-0.115470053837925,-0.8,-0.2));
#15273=CARTESIAN_POINT('Origin',(-0.115470053837925,-0.5,0.2));
#15274=CARTESIAN_POINT('',(-0.115470053837925,-0.5,0.2));
#15275=CARTESIAN_POINT('',(-0.23094010767585,-0.5,-2.82820063659975E-17));
#15276=CARTESIAN_POINT('',(-0.115470053837925,-0.8,0.2));
#15277=CARTESIAN_POINT('',(-0.115470053837925,-0.5,0.2));
#15278=CARTESIAN_POINT('',(-0.23094010767585,-0.8,-2.82820063659975E-17));
#15279=CARTESIAN_POINT('Origin',(0.115470053837925,-0.5,0.2));
#15280=CARTESIAN_POINT('',(0.115470053837925,-0.5,0.2));
#15281=CARTESIAN_POINT('',(-0.115470053837925,-0.5,0.2));
#15282=CARTESIAN_POINT('',(0.115470053837925,-0.8,0.2));
#15283=CARTESIAN_POINT('',(0.115470053837925,-0.5,0.2));
#15284=CARTESIAN_POINT('',(-0.115470053837925,-0.8,0.2));
#15285=CARTESIAN_POINT('Origin',(0.23094010767585,-0.5,0.));
#15286=CARTESIAN_POINT('',(0.115470053837925,-0.5,0.2));
#15287=CARTESIAN_POINT('',(0.115470053837925,-0.8,0.2));
#15288=CARTESIAN_POINT('Origin',(0.,-0.5,0.));
#15289=CARTESIAN_POINT('Origin',(0.,-0.8,0.));
#15290=CARTESIAN_POINT('Origin',(0.,-1.4,0.));
#15291=CARTESIAN_POINT('',(-0.24505,-1.4,3.00099698131059E-17));
#15292=CARTESIAN_POINT('Origin',(0.,-1.4,0.));
#15293=CARTESIAN_POINT('Origin',(0.375,0.5,0.));
#15294=CARTESIAN_POINT('',(-0.375,0.5,-4.59242549680257E-17));
#15295=CARTESIAN_POINT('Origin',(0.,0.5,0.));
#15296=CARTESIAN_POINT('Origin',(0.,0.475,0.));
#15297=CARTESIAN_POINT('',(-0.425,0.45,-5.20474889637625E-17));
#15298=CARTESIAN_POINT('Origin',(0.,0.45,0.));
#15299=CARTESIAN_POINT('',(-0.4,0.475,-4.89858719658941E-17));
#15300=CARTESIAN_POINT('Origin',(0.,0.24,0.));
#15301=CARTESIAN_POINT('',(-0.425,0.0299999999999998,-5.20474889637625E-17));
#15302=CARTESIAN_POINT('Origin',(0.,0.0299999999999998,0.));
#15303=CARTESIAN_POINT('',(-0.425,0.24,-5.20474889637625E-17));
#15304=CARTESIAN_POINT('Origin',(0.,0.0150000000000001,0.));
#15305=CARTESIAN_POINT('',(-0.395,4.85722573273506E-17,-4.83735485663204E-17));
#15306=CARTESIAN_POINT('Origin',(0.,0.,0.));
#15307=CARTESIAN_POINT('',(-0.41,0.0150000000000001,-5.02105187650415E-17));
#15308=CARTESIAN_POINT('Origin',(0.27,0.,0.));
#15309=CARTESIAN_POINT('',(-0.27,0.,-3.30654635769785E-17));
#15310=CARTESIAN_POINT('Origin',(0.,0.,0.));
#15311=CARTESIAN_POINT('Origin',(0.,-0.02,0.));
#15312=CARTESIAN_POINT('',(-0.24505,-0.0498999999999999,3.00099698131059E-17));
#15313=CARTESIAN_POINT('Origin',(0.,-0.0498999999999999,0.));
#15314=CARTESIAN_POINT('',(-0.26,-0.02,-3.18408167778312E-17));
#15315=CARTESIAN_POINT('Origin',(0.,-0.995,0.));
#15316=CARTESIAN_POINT('',(-0.24505,-0.995,-3.00099698131059E-17));
#17222=UNCERTAINTY_MEASURE_WITH_UNIT(LENGTH_MEASURE(0.001),#17323,
'DISTANCE_ACCURACY_VALUE',
'Maximum model space distance between geometric entities at asserted c
onnectivities');
#17261=UNCERTAINTY_MEASURE_WITH_UNIT(LENGTH_MEASURE(0.001),#17323,
'DISTANCE_ACCURACY_VALUE',
'Maximum model space distance between geometric entities at asserted c
onnectivities');
#17283=(
GEOMETRIC_REPRESENTATION_CONTEXT(3)
GLOBAL_UNCERTAINTY_ASSIGNED_CONTEXT((#17222))
GLOBAL_UNIT_ASSIGNED_CONTEXT((#17323,#17325,#17326))
REPRESENTATION_CONTEXT('','3D')
);
#17322=(
GEOMETRIC_REPRESENTATION_CONTEXT(3)
GLOBAL_UNCERTAINTY_ASSIGNED_CONTEXT((#17261))
GLOBAL_UNIT_ASSIGNED_CONTEXT((#17323,#17325,#17326))
REPRESENTATION_CONTEXT('','3D')
);
#17323=(
LENGTH_UNIT()
NAMED_UNIT(*)
SI_UNIT(.CENTI.,.METRE.)
);
#17325=(
NAMED_UNIT(*)
PLANE_ANGLE_UNIT()
SI_UNIT($,.RADIAN.)
);
#17326=(
NAMED_UNIT(*)
SI_UNIT($,.STERADIAN.)
SOLID_ANGLE_UNIT()
);
#17348=SHAPE_DEFINITION_REPRESENTATION(#17410,#17579);
#17410=PRODUCT_DEFINITION_SHAPE('',$,#17640);
#17579=SHAPE_REPRESENTATION('',(#10126),#17283);
#17618=PRODUCT_DEFINITION_CONTEXT('part definition',#17800,'design');
#17640=PRODUCT_DEFINITION('M5x14 Cap Screw','M5x14 Cap Screw',#17700,#17618);
#17700=PRODUCT_DEFINITION_FORMATION('',$,#17823);
#17800=APPLICATION_CONTEXT(
'Core Data for Automotive Mechanical Design Process');
#17801=PRODUCT_CONTEXT('part definition',#17800,'mechanical');
#17823=PRODUCT('M5x14 Cap Screw','M5x14 Cap Screw','M5x14 Cap Screw',(#17801));
#17932=COLOUR_RGB('Black',0.12,0.14,0.17);
#17933=FILL_AREA_STYLE_COLOUR('',#17932);
#17934=FILL_AREA_STYLE('',(#17933));
#17935=SURFACE_STYLE_FILL_AREA(#17934);
#17936=SURFACE_SIDE_STYLE('',(#17935));
#17937=SURFACE_STYLE_USAGE(.BOTH.,#17936);
#17938=PRESENTATION_STYLE_ASSIGNMENT((#17937));
ENDSEC;
END-ISO-10303-21;
